ISO-10303-21;
HEADER;
/* Generated by software containing ST-Developer
 * from STEP Tools, Inc. (www.steptools.com) 
 */

FILE_DESCRIPTION(
/* description */ ('PAT-091'),
/* implementation_level */ '2;1');

FILE_NAME(
/* name */ 'Axle distance sleeve 5 mm (9).step',
/* time_stamp */ '2026-10-27T15:34:44-07:00',
/* author */ (''),
/* organization */ (''),
/* preprocessor_version */ 'ST-DEVELOPER v20.2',
/* originating_system */ 'Autodesk Translation Framework v15.17.0.0',
/* authorisation */ '');

FILE_SCHEMA (('AUTOMOTIVE_DESIGN { 1 0 10303 214 3 1 1 }'));
ENDSEC;

DATA;
#10=MECHANICAL_DESIGN_GEOMETRIC_PRESENTATION_REPRESENTATION('',(#1038),#25100);
#818=SHAPE_REPRESENTATION_RELATIONSHIP('SRR','None',#25584,#928);
#928=ADVANCED_BREP_SHAPE_REPRESENTATION('',(#1160),#25054);
#1038=STYLED_ITEM('',(#26191),#1160);
#1160=MANIFOLD_SOLID_BREP('Body1',#13317);
#1514=FACE_BOUND('',#3696,.T.);
#1515=FACE_BOUND('',#3698,.T.);
#1927=PLANE('',#15635);
#1928=PLANE('',#15636);
#2576=FACE_OUTER_BOUND('',#3693,.T.);
#2577=FACE_OUTER_BOUND('',#3694,.T.);
#2578=FACE_OUTER_BOUND('',#3695,.T.);
#2579=FACE_OUTER_BOUND('',#3697,.T.);
#3693=EDGE_LOOP('',(#11020,#11021,#11022,#11023));
#3694=EDGE_LOOP('',(#11024,#11025,#11026,#11027));
#3695=EDGE_LOOP('',(#11028));
#3696=EDGE_LOOP('',(#11029));
#3697=EDGE_LOOP('',(#11030));
#3698=EDGE_LOOP('',(#11031));
#4690=LINE('',#23324,#5430);
#4691=LINE('',#23330,#5431);
#5430=VECTOR('',#19126,0.605);
#5431=VECTOR('',#19133,0.800000000000001);
#6058=CIRCLE('',#15630,0.605);
#6059=CIRCLE('',#15631,0.605);
#6060=CIRCLE('',#15633,0.800000000000001);
#6061=CIRCLE('',#15634,0.800000000000001);
#7063=VERTEX_POINT('',#23321);
#7064=VERTEX_POINT('',#23323);
#7065=VERTEX_POINT('',#23327);
#7066=VERTEX_POINT('',#23329);
#8445=EDGE_CURVE('',#7063,#7063,#6058,.T.);
#8446=EDGE_CURVE('',#7063,#7064,#4690,.T.);
#8447=EDGE_CURVE('',#7064,#7064,#6059,.T.);
#8448=EDGE_CURVE('',#7065,#7065,#6060,.T.);
#8449=EDGE_CURVE('',#7065,#7066,#4691,.T.);
#8450=EDGE_CURVE('',#7066,#7066,#6061,.T.);
#11020=ORIENTED_EDGE('',*,*,#8445,.F.);
#11021=ORIENTED_EDGE('',*,*,#8446,.T.);
#11022=ORIENTED_EDGE('',*,*,#8447,.T.);
#11023=ORIENTED_EDGE('',*,*,#8446,.F.);
#11024=ORIENTED_EDGE('',*,*,#8448,.F.);
#11025=ORIENTED_EDGE('',*,*,#8449,.T.);
#11026=ORIENTED_EDGE('',*,*,#8450,.T.);
#11027=ORIENTED_EDGE('',*,*,#8449,.F.);
#11028=ORIENTED_EDGE('',*,*,#8448,.T.);
#11029=ORIENTED_EDGE('',*,*,#8445,.T.);
#11030=ORIENTED_EDGE('',*,*,#8450,.F.);
#11031=ORIENTED_EDGE('',*,*,#8447,.F.);
#12292=CYLINDRICAL_SURFACE('',#15629,0.605);
#12293=CYLINDRICAL_SURFACE('',#15632,0.800000000000001);
#12943=ADVANCED_FACE('',(#2576),#12292,.F.);
#12944=ADVANCED_FACE('',(#2577),#12293,.T.);
#12945=ADVANCED_FACE('',(#2578,#1514),#1927,.T.);
#12946=ADVANCED_FACE('',(#2579,#1515),#1928,.F.);
#13317=CLOSED_SHELL('',(#12943,#12944,#12945,#12946));
#15628=AXIS2_PLACEMENT_3D('',#23319,#19120,#19121);
#15629=AXIS2_PLACEMENT_3D('',#23320,#19122,#19123);
#15630=AXIS2_PLACEMENT_3D('',#23322,#19124,#19125);
#15631=AXIS2_PLACEMENT_3D('',#23325,#19127,#19128);
#15632=AXIS2_PLACEMENT_3D('',#23326,#19129,#19130);
#15633=AXIS2_PLACEMENT_3D('',#23328,#19131,#19132);
#15634=AXIS2_PLACEMENT_3D('',#23331,#19134,#19135);
#15635=AXIS2_PLACEMENT_3D('',#23332,#19136,#19137);
#15636=AXIS2_PLACEMENT_3D('',#23333,#19138,#19139);
#19120=DIRECTION('axis',(0.,0.,1.));
#19121=DIRECTION('refdir',(1.,0.,0.));
#19122=DIRECTION('center_axis',(0.,1.,0.));
#19123=DIRECTION('ref_axis',(1.,0.,0.));
#19124=DIRECTION('center_axis',(0.,-1.,0.));
#19125=DIRECTION('ref_axis',(1.,0.,0.));
#19126=DIRECTION('',(0.,-1.,0.));
#19127=DIRECTION('center_axis',(0.,-1.,0.));
#19128=DIRECTION('ref_axis',(1.,0.,0.));
#19129=DIRECTION('center_axis',(0.,1.,0.));
#19130=DIRECTION('ref_axis',(1.,0.,0.));
#19131=DIRECTION('center_axis',(0.,1.,0.));
#19132=DIRECTION('ref_axis',(1.,0.,0.));
#19133=DIRECTION('',(0.,-1.,0.));
#19134=DIRECTION('center_axis',(0.,1.,0.));
#19135=DIRECTION('ref_axis',(1.,0.,0.));
#19136=DIRECTION('center_axis',(0.,1.,0.));
#19137=DIRECTION('ref_axis',(1.,0.,0.));
#19138=DIRECTION('center_axis',(0.,1.,0.));
#19139=DIRECTION('ref_axis',(1.,0.,0.));
#23319=CARTESIAN_POINT('',(0.,0.,0.));
#23320=CARTESIAN_POINT('Origin',(19.3649167310371,-7.5,8.));
#23321=CARTESIAN_POINT('',(18.7599167310371,-7.,8.));
#23322=CARTESIAN_POINT('Origin',(19.3649167310371,-7.,8.));
#23323=CARTESIAN_POINT('',(18.7599167310371,-7.5,8.));
#23324=CARTESIAN_POINT('',(18.7599167310371,-7.5,8.));
#23325=CARTESIAN_POINT('Origin',(19.3649167310371,-7.5,8.));
#23326=CARTESIAN_POINT('Origin',(19.3649167310371,-7.5,8.));
#23327=CARTESIAN_POINT('',(18.5649167310371,-7.,8.));
#23328=CARTESIAN_POINT('Origin',(19.3649167310371,-7.,8.));
#23329=CARTESIAN_POINT('',(18.5649167310371,-7.5,8.));
#23330=CARTESIAN_POINT('',(18.5649167310371,-7.5,8.));
#23331=CARTESIAN_POINT('Origin',(19.3649167310371,-7.5,8.));
#23332=CARTESIAN_POINT('Origin',(19.3649167310371,-7.,8.));
#23333=CARTESIAN_POINT('Origin',(19.3649167310371,-7.5,8.));
#24933=UNCERTAINTY_MEASURE_WITH_UNIT(LENGTH_MEASURE(0.001),#25101,
'DISTANCE_ACCURACY_VALUE',
'Maximum model space distance between geometric entities at asserted c
onnectivities');
#24979=UNCERTAINTY_MEASURE_WITH_UNIT(LENGTH_MEASURE(0.001),#25101,
'DISTANCE_ACCURACY_VALUE',
'Maximum model space distance between geometric entities at asserted c
onnectivities');
#25054=(
GEOMETRIC_REPRESENTATION_CONTEXT(3)
GLOBAL_UNCERTAINTY_ASSIGNED_CONTEXT((#24933))
GLOBAL_UNIT_ASSIGNED_CONTEXT((#25101,#25103,#25104))
REPRESENTATION_CONTEXT('','3D')
);
#25100=(
GEOMETRIC_REPRESENTATION_CONTEXT(3)
GLOBAL_UNCERTAINTY_ASSIGNED_CONTEXT((#24979))
GLOBAL_UNIT_ASSIGNED_CONTEXT((#25101,#25103,#25104))
REPRESENTATION_CONTEXT('','3D')
);
#25101=(
LENGTH_UNIT()
NAMED_UNIT(*)
SI_UNIT(.CENTI.,.METRE.)
);
#25103=(
NAMED_UNIT(*)
PLANE_ANGLE_UNIT()
SI_UNIT($,.RADIAN.)
);
#25104=(
NAMED_UNIT(*)
SI_UNIT($,.STERADIAN.)
SOLID_ANGLE_UNIT()
);
#25179=SHAPE_DEFINITION_REPRESENTATION(#25301,#25584);
#25301=PRODUCT_DEFINITION_SHAPE('',$,#25705);
#25584=SHAPE_REPRESENTATION('',(#15628),#25054);
#25630=PRODUCT_DEFINITION_CONTEXT('part definition',#25992,'design');
#25705=PRODUCT_DEFINITION('Axle distance sleeve 5 mm (9)',
'Axle distance sleeve 5 mm (9)',#25825,#25630);
#25825=PRODUCT_DEFINITION_FORMATION('',$,#26068);
#25992=APPLICATION_CONTEXT(
'Core Data for Automotive Mechanical Design Process');
#25993=PRODUCT_CONTEXT('part definition',#25992,'mechanical');
#26068=PRODUCT('Axle distance sleeve 5 mm (9)',
'Axle distance sleeve 5 mm (9)','Axle distance sleeve 5 mm (9)',(#25993));
#26185=COLOUR_RGB('Grey',0.48,0.52,0.57);
#26186=FILL_AREA_STYLE_COLOUR('',#26185);
#26187=FILL_AREA_STYLE('',(#26186));
#26188=SURFACE_STYLE_FILL_AREA(#26187);
#26189=SURFACE_SIDE_STYLE('',(#26188));
#26190=SURFACE_STYLE_USAGE(.BOTH.,#26189);
#26191=PRESENTATION_STYLE_ASSIGNMENT((#26190));
ENDSEC;
END-ISO-10303-21;
